ISO-10303-21;
HEADER;
/* Generated by software containing ST-Developer
 * from STEP Tools, Inc. (www.steptools.com) 
 */

FILE_DESCRIPTION(
/* description */ ('Four-bar tabletop demonstrator'),
/* implementation_level */ '2;1');

FILE_NAME(
/* name */ 'M4x4 collar screw.step',
/* time_stamp */ '2026-10-29T17:05:23-07:00',
/* author */ (''),
/* organization */ (''),
/* preprocessor_version */ 'ST-DEVELOPER v20.2',
/* originating_system */ 'Autodesk Translation Framework v15.17.0.0',
/* authorisation */ '');

FILE_SCHEMA (('AUTOMOTIVE_DESIGN { 1 0 10303 214 3 1 1 }'));
ENDSEC;

DATA;
#10=MECHANICAL_DESIGN_GEOMETRIC_PRESENTATION_REPRESENTATION('',(#359),#6705);
#275=CONICAL_SURFACE('',#4032,0.185,0.785398163397449);
#321=SHAPE_REPRESENTATION_RELATIONSHIP('SRR','None',#6831,#336);
#336=ADVANCED_BREP_SHAPE_REPRESENTATION('',(#380),#6704);
#359=STYLED_ITEM('',(#6996),#380);
#380=MANIFOLD_SOLID_BREP('Body1',#3405);
#461=FACE_BOUND('',#1046,.T.);
#553=PLANE('',#4021);
#554=PLANE('',#4023);
#555=PLANE('',#4024);
#556=PLANE('',#4025);
#557=PLANE('',#4026);
#558=PLANE('',#4027);
#559=PLANE('',#4028);
#560=PLANE('',#4029);
#561=PLANE('',#4030);
#754=FACE_OUTER_BOUND('',#1037,.T.);
#755=FACE_OUTER_BOUND('',#1038,.T.);
#756=FACE_OUTER_BOUND('',#1039,.T.);
#757=FACE_OUTER_BOUND('',#1040,.T.);
#758=FACE_OUTER_BOUND('',#1041,.T.);
#759=FACE_OUTER_BOUND('',#1042,.T.);
#760=FACE_OUTER_BOUND('',#1043,.T.);
#761=FACE_OUTER_BOUND('',#1044,.T.);
#762=FACE_OUTER_BOUND('',#1045,.T.);
#763=FACE_OUTER_BOUND('',#1047,.T.);
#764=FACE_OUTER_BOUND('',#1048,.T.);
#1037=EDGE_LOOP('',(#3058));
#1038=EDGE_LOOP('',(#3059,#3060,#3061,#3062));
#1039=EDGE_LOOP('',(#3063,#3064,#3065,#3066));
#1040=EDGE_LOOP('',(#3067,#3068,#3069,#3070));
#1041=EDGE_LOOP('',(#3071,#3072,#3073,#3074));
#1042=EDGE_LOOP('',(#3075,#3076,#3077,#3078));
#1043=EDGE_LOOP('',(#3079,#3080,#3081,#3082));
#1044=EDGE_LOOP('',(#3083,#3084,#3085,#3086,#3087,#3088));
#1045=EDGE_LOOP('',(#3089));
#1046=EDGE_LOOP('',(#3090,#3091,#3092,#3093,#3094,#3095));
#1047=EDGE_LOOP('',(#3096,#3097,#3098,#3099));
#1048=EDGE_LOOP('',(#3100,#3101,#3102,#3103));
#1199=LINE('',#6588,#1369);
#1200=LINE('',#6590,#1370);
#1201=LINE('',#6592,#1371);
#1202=LINE('',#6593,#1372);
#1203=LINE('',#6596,#1373);
#1204=LINE('',#6598,#1374);
#1205=LINE('',#6599,#1375);
#1206=LINE('',#6602,#1376);
#1207=LINE('',#6604,#1377);
#1208=LINE('',#6605,#1378);
#1209=LINE('',#6608,#1379);
#1210=LINE('',#6610,#1380);
#1211=LINE('',#6611,#1381);
#1212=LINE('',#6614,#1382);
#1213=LINE('',#6616,#1383);
#1214=LINE('',#6617,#1384);
#1215=LINE('',#6619,#1385);
#1216=LINE('',#6620,#1386);
#1217=LINE('',#6628,#1387);
#1218=LINE('',#6630,#1388);
#1369=VECTOR('',#5120,1.);
#1370=VECTOR('',#5121,1.);
#1371=VECTOR('',#5122,1.);
#1372=VECTOR('',#5123,1.);
#1373=VECTOR('',#5126,1.);
#1374=VECTOR('',#5127,1.);
#1375=VECTOR('',#5128,1.);
#1376=VECTOR('',#5131,1.);
#1377=VECTOR('',#5132,1.);
#1378=VECTOR('',#5133,1.);
#1379=VECTOR('',#5136,1.);
#1380=VECTOR('',#5137,1.);
#1381=VECTOR('',#5138,1.);
#1382=VECTOR('',#5141,1.);
#1383=VECTOR('',#5142,1.);
#1384=VECTOR('',#5143,1.);
#1385=VECTOR('',#5146,1.);
#1386=VECTOR('',#5147,1.);
#1387=VECTOR('',#5158,0.185);
#1388=VECTOR('',#5161,0.2);
#1597=CIRCLE('',#4022,0.1954);
#1598=CIRCLE('',#4031,0.17);
#1599=CIRCLE('',#4033,0.1954);
#1865=VERTEX_POINT('',#6583);
#1866=VERTEX_POINT('',#6586);
#1867=VERTEX_POINT('',#6587);
#1868=VERTEX_POINT('',#6589);
#1869=VERTEX_POINT('',#6591);
#1870=VERTEX_POINT('',#6595);
#1871=VERTEX_POINT('',#6597);
#1872=VERTEX_POINT('',#6601);
#1873=VERTEX_POINT('',#6603);
#1874=VERTEX_POINT('',#6607);
#1875=VERTEX_POINT('',#6609);
#1876=VERTEX_POINT('',#6613);
#1877=VERTEX_POINT('',#6615);
#1878=VERTEX_POINT('',#6623);
#1879=VERTEX_POINT('',#6626);
#2265=EDGE_CURVE('',#1865,#1865,#1597,.T.);
#2266=EDGE_CURVE('',#1866,#1867,#1199,.T.);
#2267=EDGE_CURVE('',#1866,#1868,#1200,.T.);
#2268=EDGE_CURVE('',#1868,#1869,#1201,.T.);
#2269=EDGE_CURVE('',#1867,#1869,#1202,.T.);
#2270=EDGE_CURVE('',#1870,#1866,#1203,.T.);
#2271=EDGE_CURVE('',#1870,#1871,#1204,.T.);
#2272=EDGE_CURVE('',#1871,#1868,#1205,.T.);
#2273=EDGE_CURVE('',#1872,#1870,#1206,.T.);
#2274=EDGE_CURVE('',#1872,#1873,#1207,.T.);
#2275=EDGE_CURVE('',#1873,#1871,#1208,.T.);
#2276=EDGE_CURVE('',#1874,#1872,#1209,.T.);
#2277=EDGE_CURVE('',#1874,#1875,#1210,.T.);
#2278=EDGE_CURVE('',#1875,#1873,#1211,.T.);
#2279=EDGE_CURVE('',#1876,#1874,#1212,.T.);
#2280=EDGE_CURVE('',#1876,#1877,#1213,.T.);
#2281=EDGE_CURVE('',#1877,#1875,#1214,.T.);
#2282=EDGE_CURVE('',#1867,#1876,#1215,.T.);
#2283=EDGE_CURVE('',#1869,#1877,#1216,.T.);
#2284=EDGE_CURVE('',#1878,#1878,#1598,.T.);
#2285=EDGE_CURVE('',#1879,#1879,#1599,.T.);
#2286=EDGE_CURVE('',#1879,#1878,#1217,.T.);
#2287=EDGE_CURVE('',#1865,#1879,#1218,.T.);
#3058=ORIENTED_EDGE('',*,*,#2265,.F.);
#3059=ORIENTED_EDGE('',*,*,#2266,.F.);
#3060=ORIENTED_EDGE('',*,*,#2267,.T.);
#3061=ORIENTED_EDGE('',*,*,#2268,.T.);
#3062=ORIENTED_EDGE('',*,*,#2269,.F.);
#3063=ORIENTED_EDGE('',*,*,#2270,.F.);
#3064=ORIENTED_EDGE('',*,*,#2271,.T.);
#3065=ORIENTED_EDGE('',*,*,#2272,.T.);
#3066=ORIENTED_EDGE('',*,*,#2267,.F.);
#3067=ORIENTED_EDGE('',*,*,#2273,.F.);
#3068=ORIENTED_EDGE('',*,*,#2274,.T.);
#3069=ORIENTED_EDGE('',*,*,#2275,.T.);
#3070=ORIENTED_EDGE('',*,*,#2271,.F.);
#3071=ORIENTED_EDGE('',*,*,#2276,.F.);
#3072=ORIENTED_EDGE('',*,*,#2277,.T.);
#3073=ORIENTED_EDGE('',*,*,#2278,.T.);
#3074=ORIENTED_EDGE('',*,*,#2274,.F.);
#3075=ORIENTED_EDGE('',*,*,#2279,.F.);
#3076=ORIENTED_EDGE('',*,*,#2280,.T.);
#3077=ORIENTED_EDGE('',*,*,#2281,.T.);
#3078=ORIENTED_EDGE('',*,*,#2277,.F.);
#3079=ORIENTED_EDGE('',*,*,#2282,.F.);
#3080=ORIENTED_EDGE('',*,*,#2269,.T.);
#3081=ORIENTED_EDGE('',*,*,#2283,.T.);
#3082=ORIENTED_EDGE('',*,*,#2280,.F.);
#3083=ORIENTED_EDGE('',*,*,#2283,.F.);
#3084=ORIENTED_EDGE('',*,*,#2268,.F.);
#3085=ORIENTED_EDGE('',*,*,#2272,.F.);
#3086=ORIENTED_EDGE('',*,*,#2275,.F.);
#3087=ORIENTED_EDGE('',*,*,#2278,.F.);
#3088=ORIENTED_EDGE('',*,*,#2281,.F.);
#3089=ORIENTED_EDGE('',*,*,#2284,.F.);
#3090=ORIENTED_EDGE('',*,*,#2266,.T.);
#3091=ORIENTED_EDGE('',*,*,#2282,.T.);
#3092=ORIENTED_EDGE('',*,*,#2279,.T.);
#3093=ORIENTED_EDGE('',*,*,#2276,.T.);
#3094=ORIENTED_EDGE('',*,*,#2273,.T.);
#3095=ORIENTED_EDGE('',*,*,#2270,.T.);
#3096=ORIENTED_EDGE('',*,*,#2285,.F.);
#3097=ORIENTED_EDGE('',*,*,#2286,.T.);
#3098=ORIENTED_EDGE('',*,*,#2284,.T.);
#3099=ORIENTED_EDGE('',*,*,#2286,.F.);
#3100=ORIENTED_EDGE('',*,*,#2265,.T.);
#3101=ORIENTED_EDGE('',*,*,#2287,.T.);
#3102=ORIENTED_EDGE('',*,*,#2285,.T.);
#3103=ORIENTED_EDGE('',*,*,#2287,.F.);
#3177=CYLINDRICAL_SURFACE('',#4034,0.1954);
#3370=ADVANCED_FACE('',(#754),#553,.F.);
#3371=ADVANCED_FACE('',(#755),#554,.F.);
#3372=ADVANCED_FACE('',(#756),#555,.F.);
#3373=ADVANCED_FACE('',(#757),#556,.F.);
#3374=ADVANCED_FACE('',(#758),#557,.F.);
#3375=ADVANCED_FACE('',(#759),#558,.F.);
#3376=ADVANCED_FACE('',(#760),#559,.F.);
#3377=ADVANCED_FACE('',(#761),#560,.F.);
#3378=ADVANCED_FACE('',(#762,#461),#561,.T.);
#3379=ADVANCED_FACE('',(#763),#275,.T.);
#3380=ADVANCED_FACE('',(#764),#3177,.T.);
#3405=CLOSED_SHELL('',(#3370,#3371,#3372,#3373,#3374,#3375,#3376,#3377,
#3378,#3379,#3380));
#4020=AXIS2_PLACEMENT_3D('',#6581,#5112,#5113);
#4021=AXIS2_PLACEMENT_3D('',#6582,#5114,#5115);
#4022=AXIS2_PLACEMENT_3D('',#6584,#5116,#5117);
#4023=AXIS2_PLACEMENT_3D('',#6585,#5118,#5119);
#4024=AXIS2_PLACEMENT_3D('',#6594,#5124,#5125);
#4025=AXIS2_PLACEMENT_3D('',#6600,#5129,#5130);
#4026=AXIS2_PLACEMENT_3D('',#6606,#5134,#5135);
#4027=AXIS2_PLACEMENT_3D('',#6612,#5139,#5140);
#4028=AXIS2_PLACEMENT_3D('',#6618,#5144,#5145);
#4029=AXIS2_PLACEMENT_3D('',#6621,#5148,#5149);
#4030=AXIS2_PLACEMENT_3D('',#6622,#5150,#5151);
#4031=AXIS2_PLACEMENT_3D('',#6624,#5152,#5153);
#4032=AXIS2_PLACEMENT_3D('',#6625,#5154,#5155);
#4033=AXIS2_PLACEMENT_3D('',#6627,#5156,#5157);
#4034=AXIS2_PLACEMENT_3D('',#6629,#5159,#5160);
#5112=DIRECTION('axis',(0.,0.,1.));
#5113=DIRECTION('refdir',(1.,0.,0.));
#5114=DIRECTION('center_axis',(0.,1.,0.));
#5115=DIRECTION('ref_axis',(1.,0.,0.));
#5116=DIRECTION('center_axis',(0.,1.,0.));
#5117=DIRECTION('ref_axis',(1.,0.,0.));
#5118=DIRECTION('center_axis',(0.866025403784439,0.,-0.5));
#5119=DIRECTION('ref_axis',(0.5,0.,0.866025403784439));
#5120=DIRECTION('',(0.5,0.,0.866025403784439));
#5121=DIRECTION('',(0.,-1.,0.));
#5122=DIRECTION('',(0.5,0.,0.866025403784439));
#5123=DIRECTION('',(0.,-1.,0.));
#5124=DIRECTION('center_axis',(1.20185167898973E-16,0.,-1.));
#5125=DIRECTION('ref_axis',(1.,0.,1.20185167898973E-16));
#5126=DIRECTION('',(1.,0.,1.20185167898973E-16));
#5127=DIRECTION('',(0.,-1.,0.));
#5128=DIRECTION('',(1.,0.,1.20185167898973E-16));
#5129=DIRECTION('center_axis',(-0.866025403784439,0.,-0.5));
#5130=DIRECTION('ref_axis',(0.5,0.,-0.866025403784439));
#5131=DIRECTION('',(0.5,0.,-0.866025403784439));
#5132=DIRECTION('',(0.,-1.,0.));
#5133=DIRECTION('',(0.5,0.,-0.866025403784439));
#5134=DIRECTION('center_axis',(-0.866025403784439,0.,0.5));
#5135=DIRECTION('ref_axis',(-0.5,0.,-0.866025403784439));
#5136=DIRECTION('',(-0.5,0.,-0.866025403784439));
#5137=DIRECTION('',(0.,-1.,0.));
#5138=DIRECTION('',(-0.5,0.,-0.866025403784439));
#5139=DIRECTION('center_axis',(-2.40370335797945E-16,0.,1.));
#5140=DIRECTION('ref_axis',(-1.,0.,-2.40370335797945E-16));
#5141=DIRECTION('',(-1.,0.,-2.40370335797945E-16));
#5142=DIRECTION('',(0.,-1.,0.));
#5143=DIRECTION('',(-1.,0.,-2.40370335797945E-16));
#5144=DIRECTION('center_axis',(0.866025403784439,0.,0.5));
#5145=DIRECTION('ref_axis',(-0.5,0.,0.866025403784439));
#5146=DIRECTION('',(-0.5,0.,0.866025403784439));
#5147=DIRECTION('',(-0.5,0.,0.866025403784439));
#5148=DIRECTION('center_axis',(0.,-1.,0.));
#5149=DIRECTION('ref_axis',(0.,0.,-1.));
#5150=DIRECTION('center_axis',(0.,1.,0.));
#5151=DIRECTION('ref_axis',(0.,0.,1.));
#5152=DIRECTION('center_axis',(0.,-1.,0.));
#5153=DIRECTION('ref_axis',(1.,0.,0.));
#5154=DIRECTION('center_axis',(0.,-1.,0.));
#5155=DIRECTION('ref_axis',(1.,0.,0.));
#5156=DIRECTION('center_axis',(0.,-1.,0.));
#5157=DIRECTION('ref_axis',(1.,0.,0.));
#5158=DIRECTION('',(0.707106781186548,0.707106781186547,8.65956056235494E-17));
#5159=DIRECTION('center_axis',(0.,-1.,0.));
#5160=DIRECTION('ref_axis',(1.,0.,0.));
#5161=DIRECTION('',(0.,1.,0.));
#6581=CARTESIAN_POINT('',(0.,0.,0.));
#6582=CARTESIAN_POINT('Origin',(0.,-0.4,0.));
#6583=CARTESIAN_POINT('',(-0.1954,-0.4,2.39295984553393E-17));
#6584=CARTESIAN_POINT('Origin',(0.,-0.4,0.));
#6585=CARTESIAN_POINT('Origin',(0.0577350269189626,0.,-0.1));
#6586=CARTESIAN_POINT('',(0.0577350269189626,0.,-0.1));
#6587=CARTESIAN_POINT('',(0.115470053837925,0.,0.));
#6588=CARTESIAN_POINT('',(0.0934187836487032,0.,-0.0381939203391614));
#6589=CARTESIAN_POINT('',(0.0577350269189626,-0.2,-0.1));
#6590=CARTESIAN_POINT('',(0.0577350269189626,0.,-0.1));
#6591=CARTESIAN_POINT('',(0.115470053837925,-0.2,0.));
#6592=CARTESIAN_POINT('',(0.115470053837925,-0.2,0.));
#6593=CARTESIAN_POINT('',(0.115470053837925,0.,0.));
#6594=CARTESIAN_POINT('Origin',(-0.0577350269189626,0.,-0.1));
#6595=CARTESIAN_POINT('',(-0.0577350269189626,0.,-0.1));
#6596=CARTESIAN_POINT('',(0.0561324865405187,0.,-0.1));
#6597=CARTESIAN_POINT('',(-0.0577350269189626,-0.2,-0.1));
#6598=CARTESIAN_POINT('',(-0.0577350269189626,0.,-0.1));
#6599=CARTESIAN_POINT('',(0.0577350269189626,-0.2,-0.1));
#6600=CARTESIAN_POINT('Origin',(-0.115470053837925,0.,-1.38777878078145E-17));
#6601=CARTESIAN_POINT('',(-0.115470053837925,0.,-1.41410031829988E-17));
#6602=CARTESIAN_POINT('',(-0.0797862971081845,0.,-0.0618060796608387));
#6603=CARTESIAN_POINT('',(-0.115470053837925,-0.2,-1.38777878078145E-17));
#6604=CARTESIAN_POINT('',(-0.115470053837925,0.,-1.41410031829988E-17));
#6605=CARTESIAN_POINT('',(-0.0577350269189626,-0.2,-0.1));
#6606=CARTESIAN_POINT('Origin',(-0.0577350269189626,0.,0.1));
#6607=CARTESIAN_POINT('',(-0.0577350269189626,0.,0.1));
#6608=CARTESIAN_POINT('',(-0.0509187836487033,0.,0.111806079660839));
#6609=CARTESIAN_POINT('',(-0.0577350269189626,-0.2,0.1));
#6610=CARTESIAN_POINT('',(-0.0577350269189626,0.,0.1));
#6611=CARTESIAN_POINT('',(-0.115470053837925,-0.2,-1.41410031829988E-17));
#6612=CARTESIAN_POINT('Origin',(0.0577350269189626,0.,0.1));
#6613=CARTESIAN_POINT('',(0.0577350269189626,0.,0.1));
#6614=CARTESIAN_POINT('',(0.113867513459481,0.,0.1));
#6615=CARTESIAN_POINT('',(0.0577350269189626,-0.2,0.1));
#6616=CARTESIAN_POINT('',(0.0577350269189626,0.,0.1));
#6617=CARTESIAN_POINT('',(-0.0577350269189626,-0.2,0.1));
#6618=CARTESIAN_POINT('Origin',(0.115470053837925,0.,0.));
#6619=CARTESIAN_POINT('',(0.122286297108185,0.,-0.0118060796608386));
#6620=CARTESIAN_POINT('',(0.0577350269189626,-0.2,0.1));
#6621=CARTESIAN_POINT('Origin',(0.,-0.2,0.));
#6622=CARTESIAN_POINT('Origin',(0.17,0.,0.));
#6623=CARTESIAN_POINT('',(-0.17,-8.67361737988404E-18,-2.0818995585505E-17));
#6624=CARTESIAN_POINT('Origin',(0.,0.,0.));
#6625=CARTESIAN_POINT('Origin',(0.,-0.015,0.));
#6626=CARTESIAN_POINT('',(-0.1954,-0.0254,-2.39295984553393E-17));
#6627=CARTESIAN_POINT('Origin',(0.,-0.0254,0.));
#6628=CARTESIAN_POINT('',(-0.185,-0.015,-2.2655965784226E-17));
#6629=CARTESIAN_POINT('Origin',(0.,-0.2775,0.));
#6630=CARTESIAN_POINT('',(-0.1954,-0.2775,-2.39295984553393E-17));
#6682=UNCERTAINTY_MEASURE_WITH_UNIT(LENGTH_MEASURE(0.001),#6706,
'DISTANCE_ACCURACY_VALUE',
'Maximum model space distance between geometric entities at asserted c
onnectivities');
#6683=UNCERTAINTY_MEASURE_WITH_UNIT(LENGTH_MEASURE(0.001),#6706,
'DISTANCE_ACCURACY_VALUE',
'Maximum model space distance between geometric entities at asserted c
onnectivities');
#6704=(
GEOMETRIC_REPRESENTATION_CONTEXT(3)
GLOBAL_UNCERTAINTY_ASSIGNED_CONTEXT((#6682))
GLOBAL_UNIT_ASSIGNED_CONTEXT((#6706,#6708,#6709))
REPRESENTATION_CONTEXT('','3D')
);
#6705=(
GEOMETRIC_REPRESENTATION_CONTEXT(3)
GLOBAL_UNCERTAINTY_ASSIGNED_CONTEXT((#6683))
GLOBAL_UNIT_ASSIGNED_CONTEXT((#6706,#6708,#6709))
REPRESENTATION_CONTEXT('','3D')
);
#6706=(
LENGTH_UNIT()
NAMED_UNIT(*)
SI_UNIT(.CENTI.,.METRE.)
);
#6708=(
NAMED_UNIT(*)
PLANE_ANGLE_UNIT()
SI_UNIT($,.RADIAN.)
);
#6709=(
NAMED_UNIT(*)
SI_UNIT($,.STERADIAN.)
SOLID_ANGLE_UNIT()
);
#6730=SHAPE_DEFINITION_REPRESENTATION(#6779,#6831);
#6779=PRODUCT_DEFINITION_SHAPE('',$,#6853);
#6831=SHAPE_REPRESENTATION('',(#4020),#6704);
#6832=PRODUCT_DEFINITION_CONTEXT('part definition',#6897,'design');
#6853=PRODUCT_DEFINITION('M4x4 collar screw','M4x4 collar screw',#6874,
#6832);
#6874=PRODUCT_DEFINITION_FORMATION('',$,#6919);
#6897=APPLICATION_CONTEXT(
'Core Data for Automotive Mechanical Design Process');
#6898=PRODUCT_CONTEXT('part definition',#6897,'mechanical');
#6919=PRODUCT('M4x4 collar screw','M4x4 collar screw',
'M4x4 collar screw',(#6898));
#6990=COLOUR_RGB('Black',0.12,0.14,0.17);
#6991=FILL_AREA_STYLE_COLOUR('',#6990);
#6992=FILL_AREA_STYLE('',(#6991));
#6993=SURFACE_STYLE_FILL_AREA(#6992);
#6994=SURFACE_SIDE_STYLE('',(#6993));
#6995=SURFACE_STYLE_USAGE(.BOTH.,#6994);
#6996=PRESENTATION_STYLE_ASSIGNMENT((#6995));
ENDSEC;
END-ISO-10303-21;
